ISO-10303-21;
HEADER;
/* Generated by software containing ST-Developer
 * from STEP Tools, Inc. (www.steptools.com) 
 */

FILE_DESCRIPTION(
/* description */ (''),
/* implementation_level */ '2;1');

FILE_NAME(
/* name */ 'PO9.step',
/* time_stamp */ '2026-10-06T10:18:54-07:00',
/* author */ (''),
/* organization */ (''),
/* preprocessor_version */ 'ST-DEVELOPER v20.2',
/* originating_system */ 'Autodesk Translation Framework v15.15.0.0',
/* authorisation */ '');

FILE_SCHEMA (('AUTOMOTIVE_DESIGN { 1 0 10303 214 3 1 1 }'));
ENDSEC;

DATA;
#10=MECHANICAL_DESIGN_GEOMETRIC_PRESENTATION_REPRESENTATION('',(#89),#8445);
#71=SHAPE_REPRESENTATION_RELATIONSHIP('SRR','None',#8492,#80);
#80=ADVANCED_BREP_SHAPE_REPRESENTATION('',(#98),#8444);
#89=STYLED_ITEM('',(#8537),#98);
#98=MANIFOLD_SOLID_BREP('Body1',#4010);
#751=FACE_OUTER_BOUND('',#1018,.T.);
#752=FACE_OUTER_BOUND('',#1019,.T.);
#753=FACE_OUTER_BOUND('',#1020,.T.);
#754=FACE_OUTER_BOUND('',#1021,.T.);
#755=FACE_OUTER_BOUND('',#1022,.T.);
#756=FACE_OUTER_BOUND('',#1023,.T.);
#757=FACE_OUTER_BOUND('',#1024,.T.);
#758=FACE_OUTER_BOUND('',#1025,.T.);
#759=FACE_OUTER_BOUND('',#1026,.T.);
#760=FACE_OUTER_BOUND('',#1027,.T.);
#1018=EDGE_LOOP('',(#3605,#3606,#3607,#3608));
#1019=EDGE_LOOP('',(#3609,#3610,#3611,#3612));
#1020=EDGE_LOOP('',(#3613,#3614,#3615,#3616));
#1021=EDGE_LOOP('',(#3617,#3618,#3619,#3620));
#1022=EDGE_LOOP('',(#3621,#3622,#3623,#3624));
#1023=EDGE_LOOP('',(#3625,#3626,#3627,#3628));
#1024=EDGE_LOOP('',(#3629,#3630,#3631,#3632));
#1025=EDGE_LOOP('',(#3633,#3634,#3635,#3636));
#1026=EDGE_LOOP('',(#3637,#3638,#3639,#3640,#3641,#3642,#3643,#3644));
#1027=EDGE_LOOP('',(#3645,#3646,#3647,#3648,#3649,#3650,#3651,#3652));
#1293=LINE('',#8364,#1582);
#1294=LINE('',#8366,#1583);
#1295=LINE('',#8368,#1584);
#1296=LINE('',#8369,#1585);
#1297=LINE('',#8372,#1586);
#1298=LINE('',#8374,#1587);
#1299=LINE('',#8375,#1588);
#1300=LINE('',#8378,#1589);
#1301=LINE('',#8380,#1590);
#1302=LINE('',#8381,#1591);
#1303=LINE('',#8384,#1592);
#1304=LINE('',#8386,#1593);
#1305=LINE('',#8387,#1594);
#1306=LINE('',#8390,#1595);
#1307=LINE('',#8392,#1596);
#1308=LINE('',#8393,#1597);
#1309=LINE('',#8396,#1598);
#1310=LINE('',#8398,#1599);
#1311=LINE('',#8399,#1600);
#1312=LINE('',#8402,#1601);
#1313=LINE('',#8404,#1602);
#1314=LINE('',#8405,#1603);
#1315=LINE('',#8407,#1604);
#1316=LINE('',#8408,#1605);
#1582=VECTOR('',#5538,10.);
#1583=VECTOR('',#5539,10.);
#1584=VECTOR('',#5540,10.);
#1585=VECTOR('',#5541,10.);
#1586=VECTOR('',#5544,10.);
#1587=VECTOR('',#5545,10.);
#1588=VECTOR('',#5546,10.);
#1589=VECTOR('',#5549,10.);
#1590=VECTOR('',#5550,10.);
#1591=VECTOR('',#5551,10.);
#1592=VECTOR('',#5554,10.);
#1593=VECTOR('',#5555,10.);
#1594=VECTOR('',#5556,10.);
#1595=VECTOR('',#5559,10.);
#1596=VECTOR('',#5560,10.);
#1597=VECTOR('',#5561,10.);
#1598=VECTOR('',#5564,10.);
#1599=VECTOR('',#5565,10.);
#1600=VECTOR('',#5566,10.);
#1601=VECTOR('',#5569,10.);
#1602=VECTOR('',#5570,10.);
#1603=VECTOR('',#5571,10.);
#1604=VECTOR('',#5574,10.);
#1605=VECTOR('',#5575,10.);
#1948=VERTEX_POINT('',#8362);
#1949=VERTEX_POINT('',#8363);
#1950=VERTEX_POINT('',#8365);
#1951=VERTEX_POINT('',#8367);
#1952=VERTEX_POINT('',#8371);
#1953=VERTEX_POINT('',#8373);
#1954=VERTEX_POINT('',#8377);
#1955=VERTEX_POINT('',#8379);
#1956=VERTEX_POINT('',#8383);
#1957=VERTEX_POINT('',#8385);
#1958=VERTEX_POINT('',#8389);
#1959=VERTEX_POINT('',#8391);
#1960=VERTEX_POINT('',#8395);
#1961=VERTEX_POINT('',#8397);
#1962=VERTEX_POINT('',#8401);
#1963=VERTEX_POINT('',#8403);
#2503=EDGE_CURVE('',#1948,#1949,#1293,.T.);
#2504=EDGE_CURVE('',#1948,#1950,#1294,.T.);
#2505=EDGE_CURVE('',#1951,#1950,#1295,.T.);
#2506=EDGE_CURVE('',#1949,#1951,#1296,.T.);
#2507=EDGE_CURVE('',#1952,#1949,#1297,.T.);
#2508=EDGE_CURVE('',#1953,#1951,#1298,.T.);
#2509=EDGE_CURVE('',#1952,#1953,#1299,.T.);
#2510=EDGE_CURVE('',#1954,#1952,#1300,.T.);
#2511=EDGE_CURVE('',#1955,#1953,#1301,.T.);
#2512=EDGE_CURVE('',#1954,#1955,#1302,.T.);
#2513=EDGE_CURVE('',#1956,#1954,#1303,.T.);
#2514=EDGE_CURVE('',#1957,#1955,#1304,.T.);
#2515=EDGE_CURVE('',#1956,#1957,#1305,.T.);
#2516=EDGE_CURVE('',#1958,#1956,#1306,.T.);
#2517=EDGE_CURVE('',#1959,#1957,#1307,.T.);
#2518=EDGE_CURVE('',#1958,#1959,#1308,.T.);
#2519=EDGE_CURVE('',#1960,#1958,#1309,.T.);
#2520=EDGE_CURVE('',#1961,#1959,#1310,.T.);
#2521=EDGE_CURVE('',#1960,#1961,#1311,.T.);
#2522=EDGE_CURVE('',#1962,#1960,#1312,.T.);
#2523=EDGE_CURVE('',#1963,#1961,#1313,.T.);
#2524=EDGE_CURVE('',#1962,#1963,#1314,.T.);
#2525=EDGE_CURVE('',#1948,#1962,#1315,.T.);
#2526=EDGE_CURVE('',#1950,#1963,#1316,.T.);
#3605=ORIENTED_EDGE('',*,*,#2503,.F.);
#3606=ORIENTED_EDGE('',*,*,#2504,.T.);
#3607=ORIENTED_EDGE('',*,*,#2505,.F.);
#3608=ORIENTED_EDGE('',*,*,#2506,.F.);
#3609=ORIENTED_EDGE('',*,*,#2507,.T.);
#3610=ORIENTED_EDGE('',*,*,#2506,.T.);
#3611=ORIENTED_EDGE('',*,*,#2508,.F.);
#3612=ORIENTED_EDGE('',*,*,#2509,.F.);
#3613=ORIENTED_EDGE('',*,*,#2510,.T.);
#3614=ORIENTED_EDGE('',*,*,#2509,.T.);
#3615=ORIENTED_EDGE('',*,*,#2511,.F.);
#3616=ORIENTED_EDGE('',*,*,#2512,.F.);
#3617=ORIENTED_EDGE('',*,*,#2513,.T.);
#3618=ORIENTED_EDGE('',*,*,#2512,.T.);
#3619=ORIENTED_EDGE('',*,*,#2514,.F.);
#3620=ORIENTED_EDGE('',*,*,#2515,.F.);
#3621=ORIENTED_EDGE('',*,*,#2516,.T.);
#3622=ORIENTED_EDGE('',*,*,#2515,.T.);
#3623=ORIENTED_EDGE('',*,*,#2517,.F.);
#3624=ORIENTED_EDGE('',*,*,#2518,.F.);
#3625=ORIENTED_EDGE('',*,*,#2519,.T.);
#3626=ORIENTED_EDGE('',*,*,#2518,.T.);
#3627=ORIENTED_EDGE('',*,*,#2520,.F.);
#3628=ORIENTED_EDGE('',*,*,#2521,.F.);
#3629=ORIENTED_EDGE('',*,*,#2522,.T.);
#3630=ORIENTED_EDGE('',*,*,#2521,.T.);
#3631=ORIENTED_EDGE('',*,*,#2523,.F.);
#3632=ORIENTED_EDGE('',*,*,#2524,.F.);
#3633=ORIENTED_EDGE('',*,*,#2525,.T.);
#3634=ORIENTED_EDGE('',*,*,#2524,.T.);
#3635=ORIENTED_EDGE('',*,*,#2526,.F.);
#3636=ORIENTED_EDGE('',*,*,#2504,.F.);
#3637=ORIENTED_EDGE('',*,*,#2526,.T.);
#3638=ORIENTED_EDGE('',*,*,#2523,.T.);
#3639=ORIENTED_EDGE('',*,*,#2520,.T.);
#3640=ORIENTED_EDGE('',*,*,#2517,.T.);
#3641=ORIENTED_EDGE('',*,*,#2514,.T.);
#3642=ORIENTED_EDGE('',*,*,#2511,.T.);
#3643=ORIENTED_EDGE('',*,*,#2508,.T.);
#3644=ORIENTED_EDGE('',*,*,#2505,.T.);
#3645=ORIENTED_EDGE('',*,*,#2525,.F.);
#3646=ORIENTED_EDGE('',*,*,#2503,.T.);
#3647=ORIENTED_EDGE('',*,*,#2507,.F.);
#3648=ORIENTED_EDGE('',*,*,#2510,.F.);
#3649=ORIENTED_EDGE('',*,*,#2513,.F.);
#3650=ORIENTED_EDGE('',*,*,#2516,.F.);
#3651=ORIENTED_EDGE('',*,*,#2519,.F.);
#3652=ORIENTED_EDGE('',*,*,#2522,.F.);
#3757=PLANE('',#4490);
#3758=PLANE('',#4491);
#3759=PLANE('',#4492);
#3760=PLANE('',#4493);
#3761=PLANE('',#4494);
#3762=PLANE('',#4495);
#3763=PLANE('',#4496);
#3764=PLANE('',#4497);
#3765=PLANE('',#4498);
#3766=PLANE('',#4499);
#3992=ADVANCED_FACE('',(#751),#3757,.T.);
#3993=ADVANCED_FACE('',(#752),#3758,.T.);
#3994=ADVANCED_FACE('',(#753),#3759,.T.);
#3995=ADVANCED_FACE('',(#754),#3760,.T.);
#3996=ADVANCED_FACE('',(#755),#3761,.T.);
#3997=ADVANCED_FACE('',(#756),#3762,.T.);
#3998=ADVANCED_FACE('',(#757),#3763,.T.);
#3999=ADVANCED_FACE('',(#758),#3764,.T.);
#4000=ADVANCED_FACE('',(#759),#3765,.T.);
#4001=ADVANCED_FACE('',(#760),#3766,.F.);
#4010=CLOSED_SHELL('',(#3992,#3993,#3994,#3995,#3996,#3997,#3998,#3999,
#4000,#4001));
#4489=AXIS2_PLACEMENT_3D('',#8360,#5534,#5535);
#4490=AXIS2_PLACEMENT_3D('',#8361,#5536,#5537);
#4491=AXIS2_PLACEMENT_3D('',#8370,#5542,#5543);
#4492=AXIS2_PLACEMENT_3D('',#8376,#5547,#5548);
#4493=AXIS2_PLACEMENT_3D('',#8382,#5552,#5553);
#4494=AXIS2_PLACEMENT_3D('',#8388,#5557,#5558);
#4495=AXIS2_PLACEMENT_3D('',#8394,#5562,#5563);
#4496=AXIS2_PLACEMENT_3D('',#8400,#5567,#5568);
#4497=AXIS2_PLACEMENT_3D('',#8406,#5572,#5573);
#4498=AXIS2_PLACEMENT_3D('',#8409,#5576,#5577);
#4499=AXIS2_PLACEMENT_3D('',#8410,#5578,#5579);
#5534=DIRECTION('axis',(0.,0.,1.));
#5535=DIRECTION('refdir',(1.,0.,0.));
#5536=DIRECTION('center_axis',(1.,0.,0.));
#5537=DIRECTION('ref_axis',(0.,1.,0.));
#5538=DIRECTION('',(0.,-1.,0.));
#5539=DIRECTION('',(0.,0.,1.));
#5540=DIRECTION('',(0.,1.,0.));
#5541=DIRECTION('',(0.,0.,1.));
#5542=DIRECTION('center_axis',(0.,-1.,0.));
#5543=DIRECTION('ref_axis',(1.,0.,0.));
#5544=DIRECTION('',(1.,0.,0.));
#5545=DIRECTION('',(1.,0.,0.));
#5546=DIRECTION('',(0.,0.,1.));
#5547=DIRECTION('center_axis',(-1.,0.,0.));
#5548=DIRECTION('ref_axis',(0.,-1.,0.));
#5549=DIRECTION('',(0.,-1.,0.));
#5550=DIRECTION('',(0.,-1.,0.));
#5551=DIRECTION('',(0.,0.,1.));
#5552=DIRECTION('center_axis',(0.,1.,0.));
#5553=DIRECTION('ref_axis',(-1.,0.,0.));
#5554=DIRECTION('',(-1.,0.,0.));
#5555=DIRECTION('',(-1.,0.,0.));
#5556=DIRECTION('',(0.,0.,1.));
#5557=DIRECTION('center_axis',(1.,0.,0.));
#5558=DIRECTION('ref_axis',(0.,1.,0.));
#5559=DIRECTION('',(0.,1.,0.));
#5560=DIRECTION('',(0.,1.,0.));
#5561=DIRECTION('',(0.,0.,1.));
#5562=DIRECTION('center_axis',(0.,-1.,0.));
#5563=DIRECTION('ref_axis',(1.,0.,0.));
#5564=DIRECTION('',(1.,0.,0.));
#5565=DIRECTION('',(1.,0.,0.));
#5566=DIRECTION('',(0.,0.,1.));
#5567=DIRECTION('center_axis',(-1.,0.,0.));
#5568=DIRECTION('ref_axis',(0.,-1.,0.));
#5569=DIRECTION('',(0.,-1.,0.));
#5570=DIRECTION('',(0.,-1.,0.));
#5571=DIRECTION('',(0.,0.,1.));
#5572=DIRECTION('center_axis',(0.,-1.,0.));
#5573=DIRECTION('ref_axis',(1.,0.,0.));
#5574=DIRECTION('',(1.,0.,0.));
#5575=DIRECTION('',(1.,0.,0.));
#5576=DIRECTION('center_axis',(0.,0.,1.));
#5577=DIRECTION('ref_axis',(1.,0.,0.));
#5578=DIRECTION('center_axis',(0.,0.,1.));
#5579=DIRECTION('ref_axis',(1.,0.,0.));
#8360=CARTESIAN_POINT('',(0.,0.,0.));
#8361=CARTESIAN_POINT('Origin',(27.9999995231628,0.,0.));
#8362=CARTESIAN_POINT('',(27.9999995231628,4.4,0.));
#8363=CARTESIAN_POINT('',(27.9999995231628,0.,0.));
#8364=CARTESIAN_POINT('',(27.9999995231628,4.4,0.));
#8365=CARTESIAN_POINT('',(27.9999995231628,4.4,5.6));
#8366=CARTESIAN_POINT('',(27.9999995231628,4.4,0.));
#8367=CARTESIAN_POINT('',(27.9999995231628,0.,5.6));
#8368=CARTESIAN_POINT('',(27.9999995231628,4.4,5.6));
#8369=CARTESIAN_POINT('',(27.9999995231628,0.,0.));
#8370=CARTESIAN_POINT('Origin',(0.,0.,0.));
#8371=CARTESIAN_POINT('',(0.,0.,0.));
#8372=CARTESIAN_POINT('',(0.,0.,0.));
#8373=CARTESIAN_POINT('',(0.,0.,5.6));
#8374=CARTESIAN_POINT('',(0.,0.,5.6));
#8375=CARTESIAN_POINT('',(0.,0.,0.));
#8376=CARTESIAN_POINT('Origin',(0.,8.6,0.));
#8377=CARTESIAN_POINT('',(0.,8.6,0.));
#8378=CARTESIAN_POINT('',(0.,8.6,0.));
#8379=CARTESIAN_POINT('',(0.,8.6,5.6));
#8380=CARTESIAN_POINT('',(0.,8.6,5.6));
#8381=CARTESIAN_POINT('',(0.,8.6,0.));
#8382=CARTESIAN_POINT('Origin',(60.,8.6,0.));
#8383=CARTESIAN_POINT('',(60.,8.6,0.));
#8384=CARTESIAN_POINT('',(60.,8.6,0.));
#8385=CARTESIAN_POINT('',(60.,8.6,5.6));
#8386=CARTESIAN_POINT('',(60.,8.6,5.6));
#8387=CARTESIAN_POINT('',(60.,8.6,0.));
#8388=CARTESIAN_POINT('Origin',(60.,0.,0.));
#8389=CARTESIAN_POINT('',(60.,0.,0.));
#8390=CARTESIAN_POINT('',(60.,0.,0.));
#8391=CARTESIAN_POINT('',(60.,0.,5.6));
#8392=CARTESIAN_POINT('',(60.,0.,5.6));
#8393=CARTESIAN_POINT('',(60.,0.,0.));
#8394=CARTESIAN_POINT('Origin',(32.0000004768372,0.,0.));
#8395=CARTESIAN_POINT('',(32.0000004768372,0.,0.));
#8396=CARTESIAN_POINT('',(32.0000004768372,0.,0.));
#8397=CARTESIAN_POINT('',(32.0000004768372,0.,5.6));
#8398=CARTESIAN_POINT('',(32.0000004768372,0.,5.6));
#8399=CARTESIAN_POINT('',(32.0000004768372,0.,0.));
#8400=CARTESIAN_POINT('Origin',(32.0000004768372,4.4,0.));
#8401=CARTESIAN_POINT('',(32.0000004768372,4.4,0.));
#8402=CARTESIAN_POINT('',(32.0000004768372,4.4,0.));
#8403=CARTESIAN_POINT('',(32.0000004768372,4.4,5.6));
#8404=CARTESIAN_POINT('',(32.0000004768372,4.4,5.6));
#8405=CARTESIAN_POINT('',(32.0000004768372,4.4,0.));
#8406=CARTESIAN_POINT('Origin',(27.9999995231628,4.4,0.));
#8407=CARTESIAN_POINT('',(27.9999995231628,4.4,0.));
#8408=CARTESIAN_POINT('',(27.9999995231628,4.4,5.6));
#8409=CARTESIAN_POINT('Origin',(30.,4.3,5.6));
#8410=CARTESIAN_POINT('Origin',(30.,4.3,0.));
#8433=UNCERTAINTY_MEASURE_WITH_UNIT(LENGTH_MEASURE(0.01),#8446,
'DISTANCE_ACCURACY_VALUE',
'Maximum model space distance between geometric entities at asserted c
onnectivities');
#8434=UNCERTAINTY_MEASURE_WITH_UNIT(LENGTH_MEASURE(0.01),#8446,
'DISTANCE_ACCURACY_VALUE',
'Maximum model space distance between geometric entities at asserted c
onnectivities');
#8444=(
GEOMETRIC_REPRESENTATION_CONTEXT(3)
GLOBAL_UNCERTAINTY_ASSIGNED_CONTEXT((#8433))
GLOBAL_UNIT_ASSIGNED_CONTEXT((#8446,#8448,#8449))
REPRESENTATION_CONTEXT('','3D')
);
#8445=(
GEOMETRIC_REPRESENTATION_CONTEXT(3)
GLOBAL_UNCERTAINTY_ASSIGNED_CONTEXT((#8434))
GLOBAL_UNIT_ASSIGNED_CONTEXT((#8446,#8448,#8449))
REPRESENTATION_CONTEXT('','3D')
);
#8446=(
LENGTH_UNIT()
NAMED_UNIT(*)
SI_UNIT(.MILLI.,.METRE.)
);
#8448=(
NAMED_UNIT(*)
PLANE_ANGLE_UNIT()
SI_UNIT($,.RADIAN.)
);
#8449=(
NAMED_UNIT(*)
SI_UNIT($,.STERADIAN.)
SOLID_ANGLE_UNIT()
);
#8459=SHAPE_DEFINITION_REPRESENTATION(#8469,#8492);
#8469=PRODUCT_DEFINITION_SHAPE('',$,#8503);
#8492=SHAPE_REPRESENTATION('',(#4489),#8444);
#8493=PRODUCT_DEFINITION_CONTEXT('part definition',#8525,'design');
#8503=PRODUCT_DEFINITION('2026-10-05-11-51-31-362','PO9',#8513,#8493);
#8513=PRODUCT_DEFINITION_FORMATION('',$,#8536);
#8525=APPLICATION_CONTEXT(
'Core Data for Automotive Mechanical Design Process');
#8526=PRODUCT_CONTEXT('part definition',#8525,'mechanical');
#8536=PRODUCT('2026-10-05-11-51-31-362','PO9',$,(#8526));
#8537=PRESENTATION_STYLE_ASSIGNMENT((#8538));
#8538=SURFACE_STYLE_USAGE(.BOTH.,#8539);
#8539=SURFACE_SIDE_STYLE('',(#8540));
#8540=SURFACE_STYLE_FILL_AREA(#8541);
#8541=FILL_AREA_STYLE('Steel - Satin',(#8542));
#8542=FILL_AREA_STYLE_COLOUR('Steel - Satin',#8543);
#8543=COLOUR_RGB('Steel - Satin', 0.09019608, 0.27058824, 0.51372549);
ENDSEC;
END-ISO-10303-21;
